ISO-10303-21;
HEADER;
/* Generated by software containing ST-Developer
 * from STEP Tools, Inc. (www.steptools.com) 
 */

FILE_DESCRIPTION(
/* description */ (''),
/* implementation_level */ '2;1');

FILE_NAME(
/* name */ 'Binding Head Screw JIS B 1111 - M2x6 Steel 4.6 Plain v1 (1).step',
/* time_stamp */ '2026-10-07T02:13:48+06:00',
/* author */ (''),
/* organization */ (''),
/* preprocessor_version */ 'ST-DEVELOPER v20.2',
/* originating_system */ 'Autodesk Translation Framework v15.15.0.0',
/* authorisation */ '');

FILE_SCHEMA (('AUTOMOTIVE_DESIGN { 1 0 10303 214 3 1 1 }'));
ENDSEC;

DATA;
#10=MECHANICAL_DESIGN_GEOMETRIC_PRESENTATION_REPRESENTATION('',(#125),#17042);
#68=CONICAL_SURFACE('',#9229,0.919615242270664,0.261799387799148);
#69=CONICAL_SURFACE('',#9238,2.11281731799709,0.0872664626099693);
#101=SHAPE_REPRESENTATION_RELATIONSHIP('SRR','None',#17097,#113);
#113=ADVANCED_BREP_SHAPE_REPRESENTATION('',(#137),#17041);
#125=STYLED_ITEM('',(#17154),#137);
#137=MANIFOLD_SOLID_BREP('Body1',#8126);
#177=FACE_BOUND('',#1463,.T.);
#213=SPHERICAL_SURFACE('',#9234,6.32965591734106);
#236=TOROIDAL_SURFACE('',#9221,0.939230484541328,0.1);
#276=ELLIPSE('',#9180,0.992,0.496);
#277=ELLIPSE('',#9182,0.992,0.496);
#278=ELLIPSE('',#9187,0.992,0.496);
#279=ELLIPSE('',#9192,0.992,0.496);
#280=ELLIPSE('',#9197,0.992,0.496);
#281=ELLIPSE('',#9201,0.992,0.496);
#282=ELLIPSE('',#9203,0.992,0.496);
#283=ELLIPSE('',#9208,0.992,0.496);
#461=PLANE('',#9183);
#462=PLANE('',#9185);
#463=PLANE('',#9188);
#464=PLANE('',#9193);
#465=PLANE('',#9195);
#466=PLANE('',#9198);
#467=PLANE('',#9204);
#468=PLANE('',#9209);
#469=PLANE('',#9211);
#470=PLANE('',#9213);
#471=PLANE('',#9216);
#472=PLANE('',#9218);
#473=PLANE('',#9220);
#474=PLANE('',#9225);
#475=PLANE('',#9233);
#928=FACE_OUTER_BOUND('',#1444,.T.);
#929=FACE_OUTER_BOUND('',#1445,.T.);
#930=FACE_OUTER_BOUND('',#1446,.T.);
#931=FACE_OUTER_BOUND('',#1447,.T.);
#932=FACE_OUTER_BOUND('',#1448,.T.);
#933=FACE_OUTER_BOUND('',#1449,.T.);
#934=FACE_OUTER_BOUND('',#1450,.T.);
#935=FACE_OUTER_BOUND('',#1451,.T.);
#936=FACE_OUTER_BOUND('',#1452,.T.);
#937=FACE_OUTER_BOUND('',#1453,.T.);
#938=FACE_OUTER_BOUND('',#1454,.T.);
#939=FACE_OUTER_BOUND('',#1455,.T.);
#940=FACE_OUTER_BOUND('',#1456,.T.);
#941=FACE_OUTER_BOUND('',#1457,.T.);
#942=FACE_OUTER_BOUND('',#1458,.T.);
#943=FACE_OUTER_BOUND('',#1459,.T.);
#944=FACE_OUTER_BOUND('',#1460,.T.);
#945=FACE_OUTER_BOUND('',#1461,.T.);
#946=FACE_OUTER_BOUND('',#1462,.T.);
#947=FACE_OUTER_BOUND('',#1464,.T.);
#948=FACE_OUTER_BOUND('',#1465,.T.);
#949=FACE_OUTER_BOUND('',#1466,.T.);
#950=FACE_OUTER_BOUND('',#1467,.T.);
#951=FACE_OUTER_BOUND('',#1468,.T.);
#952=FACE_OUTER_BOUND('',#1469,.T.);
#1444=EDGE_LOOP('',(#7317,#7318,#7319,#7320,#7321,#7322));
#1445=EDGE_LOOP('',(#7323,#7324,#7325));
#1446=EDGE_LOOP('',(#7326,#7327,#7328,#7329,#7330,#7331));
#1447=EDGE_LOOP('',(#7332,#7333,#7334));
#1448=EDGE_LOOP('',(#7335,#7336,#7337,#7338,#7339,#7340));
#1449=EDGE_LOOP('',(#7341,#7342,#7343));
#1450=EDGE_LOOP('',(#7344,#7345,#7346,#7347,#7348,#7349));
#1451=EDGE_LOOP('',(#7350,#7351,#7352));
#1452=EDGE_LOOP('',(#7353,#7354,#7355,#7356,#7357,#7358));
#1453=EDGE_LOOP('',(#7359,#7360,#7361));
#1454=EDGE_LOOP('',(#7362,#7363,#7364,#7365,#7366,#7367));
#1455=EDGE_LOOP('',(#7368,#7369,#7370));
#1456=EDGE_LOOP('',(#7371,#7372,#7373));
#1457=EDGE_LOOP('',(#7374,#7375,#7376,#7377,#7378,#7379,#7380));
#1458=EDGE_LOOP('',(#7381,#7382,#7383));
#1459=EDGE_LOOP('',(#7384,#7385,#7386,#7387,#7388,#7389));
#1460=EDGE_LOOP('',(#7390,#7391,#7392,#7393,#7394,#7395,#7396,#7397));
#1461=EDGE_LOOP('',(#7398,#7399,#7400,#7401));
#1462=EDGE_LOOP('',(#7402));
#1463=EDGE_LOOP('',(#7403));
#1464=EDGE_LOOP('',(#7404,#7405,#7406,#7407));
#1465=EDGE_LOOP('',(#7408,#7409,#7410,#7411));
#1466=EDGE_LOOP('',(#7412,#7413,#7414,#7415));
#1467=EDGE_LOOP('',(#7416));
#1468=EDGE_LOOP('',(#7417,#7418,#7419,#7420,#7421,#7422,#7423,#7424,#7425,
#7426,#7427,#7428,#7429,#7430,#7431,#7432,#7433,#7434,#7435,#7436,#7437));
#1469=EDGE_LOOP('',(#7438,#7439,#7440,#7441,#7442));
#1923=CIRCLE('',#9181,0.496);
#1924=CIRCLE('',#9184,6.32479565138939);
#1925=CIRCLE('',#9186,5.93049029404341);
#1926=CIRCLE('',#9189,6.32479565138933);
#1927=CIRCLE('',#9191,0.496);
#1928=CIRCLE('',#9194,6.32479565138941);
#1929=CIRCLE('',#9196,5.93049029404341);
#1930=CIRCLE('',#9199,6.32479565138941);
#1931=CIRCLE('',#9202,0.496);
#1932=CIRCLE('',#9205,6.32479565138943);
#1933=CIRCLE('',#9207,0.496);
#1934=CIRCLE('',#9210,6.32479565138944);
#1935=CIRCLE('',#9212,6.32479565138933);
#1936=CIRCLE('',#9214,5.93049029404347);
#1937=CIRCLE('',#9215,5.93049029404347);
#1938=CIRCLE('',#9217,6.32479565138944);
#1939=CIRCLE('',#9219,5.93049029404341);
#1940=CIRCLE('',#9222,0.939230484541328);
#1941=CIRCLE('',#9223,0.1);
#1942=CIRCLE('',#9224,0.839230484541328);
#1943=CIRCLE('',#9226,2.15);
#1944=CIRCLE('',#9228,0.839230484541328);
#1945=CIRCLE('',#9230,0.96675);
#1946=CIRCLE('',#9232,0.96675);
#1947=CIRCLE('',#9235,6.32965591734106);
#1948=CIRCLE('',#9236,2.07563463599418);
#1949=CIRCLE('',#9237,2.07563463599418);
#2018=B_SPLINE_CURVE_WITH_KNOTS('',3,(#16821,#16822,#16823,#16824,#16825,
#16826,#16827,#16828,#16829,#16830,#16831,#16832,#16833,#16834,#16835),
 .UNSPECIFIED.,.F.,.F.,(4,2,2,3,2,2,4),(-0.0374758352523592,-0.0373394553501654,
-0.0186697276750827,0.,0.0186697276750831,0.0373394553501661,0.0374758352523223),
 .UNSPECIFIED.);
#2019=B_SPLINE_CURVE_WITH_KNOTS('',3,(#16863,#16864,#16865,#16866,#16867,
#16868,#16869,#16870,#16871,#16872,#16873,#16874,#16875,#16876,#16877),
 .UNSPECIFIED.,.F.,.F.,(4,2,2,3,2,2,4),(-0.0374758352523656,-0.0373394553501654,
-0.0186697276750827,0.,0.0186697276750831,0.0373394553501662,0.0374758352523289),
 .UNSPECIFIED.);
#2020=B_SPLINE_CURVE_WITH_KNOTS('',3,(#16902,#16903,#16904,#16905,#16906,
#16907,#16908,#16909,#16910,#16911,#16912,#16913,#16914,#16915,#16916),
 .UNSPECIFIED.,.F.,.F.,(4,2,2,3,2,2,4),(-0.0374758352524519,-0.0373394553501659,
-0.0186697276750829,0.,0.0186697276750829,0.0373394553501658,0.0374758352524142),
 .UNSPECIFIED.);
#2021=B_SPLINE_CURVE_WITH_KNOTS('',3,(#16932,#16933,#16934,#16935,#16936,
#16937,#16938,#16939,#16940,#16941,#16942,#16943,#16944,#16945,#16946),
 .UNSPECIFIED.,.F.,.F.,(4,2,2,3,2,2,4),(-0.0374758352524171,-0.0373394553501658,
-0.0186697276750829,0.,0.018669727675083,0.037339455350166,0.0374758352523797),
 .UNSPECIFIED.);
#2576=LINE('',#16837,#3154);
#2577=LINE('',#16844,#3155);
#2578=LINE('',#16848,#3156);
#2579=LINE('',#16853,#3157);
#2580=LINE('',#16856,#3158);
#2581=LINE('',#16860,#3159);
#2582=LINE('',#16882,#3160);
#2583=LINE('',#16886,#3161);
#2584=LINE('',#16891,#3162);
#2585=LINE('',#16894,#3163);
#2586=LINE('',#16898,#3164);
#2587=LINE('',#16918,#3165);
#2588=LINE('',#16925,#3166);
#2589=LINE('',#16929,#3167);
#2590=LINE('',#16951,#3168);
#2591=LINE('',#16955,#3169);
#2592=LINE('',#16959,#3170);
#2593=LINE('',#16963,#3171);
#2594=LINE('',#16968,#3172);
#2595=LINE('',#16971,#3173);
#2596=LINE('',#16985,#3174);
#2597=LINE('',#16989,#3175);
#2598=LINE('',#16993,#3176);
#2599=LINE('',#17002,#3177);
#3154=VECTOR('',#11645,10.);
#3155=VECTOR('',#11652,10.);
#3156=VECTOR('',#11657,10.);
#3157=VECTOR('',#11662,10.);
#3158=VECTOR('',#11665,10.);
#3159=VECTOR('',#11670,10.);
#3160=VECTOR('',#11677,10.);
#3161=VECTOR('',#11682,10.);
#3162=VECTOR('',#11687,10.);
#3163=VECTOR('',#11690,10.);
#3164=VECTOR('',#11695,10.);
#3165=VECTOR('',#11698,10.);
#3166=VECTOR('',#11705,10.);
#3167=VECTOR('',#11710,10.);
#3168=VECTOR('',#11717,10.);
#3169=VECTOR('',#11722,10.);
#3170=VECTOR('',#11727,10.);
#3171=VECTOR('',#11732,10.);
#3172=VECTOR('',#11739,10.);
#3173=VECTOR('',#11744,10.);
#3174=VECTOR('',#11763,0.839230484541328);
#3175=VECTOR('',#11768,0.919615242270664);
#3176=VECTOR('',#11773,1.);
#3177=VECTOR('',#11786,2.11281731799709);
#3871=VERTEX_POINT('',#16819);
#3872=VERTEX_POINT('',#16820);
#3873=VERTEX_POINT('',#16836);
#3874=VERTEX_POINT('',#16838);
#3875=VERTEX_POINT('',#16840);
#3876=VERTEX_POINT('',#16842);
#3877=VERTEX_POINT('',#16846);
#3878=VERTEX_POINT('',#16850);
#3879=VERTEX_POINT('',#16852);
#3880=VERTEX_POINT('',#16854);
#3881=VERTEX_POINT('',#16858);
#3882=VERTEX_POINT('',#16862);
#3883=VERTEX_POINT('',#16878);
#3884=VERTEX_POINT('',#16880);
#3885=VERTEX_POINT('',#16884);
#3886=VERTEX_POINT('',#16888);
#3887=VERTEX_POINT('',#16890);
#3888=VERTEX_POINT('',#16892);
#3889=VERTEX_POINT('',#16896);
#3890=VERTEX_POINT('',#16900);
#3891=VERTEX_POINT('',#16901);
#3892=VERTEX_POINT('',#16917);
#3893=VERTEX_POINT('',#16919);
#3894=VERTEX_POINT('',#16921);
#3895=VERTEX_POINT('',#16923);
#3896=VERTEX_POINT('',#16927);
#3897=VERTEX_POINT('',#16931);
#3898=VERTEX_POINT('',#16947);
#3899=VERTEX_POINT('',#16949);
#3900=VERTEX_POINT('',#16953);
#3901=VERTEX_POINT('',#16957);
#3902=VERTEX_POINT('',#16961);
#3903=VERTEX_POINT('',#16966);
#3904=VERTEX_POINT('',#16974);
#3905=VERTEX_POINT('',#16976);
#3906=VERTEX_POINT('',#16980);
#3907=VERTEX_POINT('',#16983);
#3908=VERTEX_POINT('',#16987);
#3909=VERTEX_POINT('',#16991);
#3910=VERTEX_POINT('',#16996);
#3911=VERTEX_POINT('',#16998);
#5026=EDGE_CURVE('',#3871,#3872,#2018,.T.);
#5027=EDGE_CURVE('',#3873,#3871,#2576,.T.);
#5028=EDGE_CURVE('',#3873,#3874,#276,.F.);
#5029=EDGE_CURVE('',#3874,#3875,#1923,.F.);
#5030=EDGE_CURVE('',#3876,#3875,#277,.T.);
#5031=EDGE_CURVE('',#3872,#3876,#2577,.T.);
#5032=EDGE_CURVE('',#3872,#3877,#1924,.T.);
#5033=EDGE_CURVE('',#3877,#3876,#2578,.F.);
#5034=EDGE_CURVE('',#3877,#3878,#1925,.T.);
#5035=EDGE_CURVE('',#3875,#3879,#2579,.F.);
#5036=EDGE_CURVE('',#3880,#3879,#278,.F.);
#5037=EDGE_CURVE('',#3878,#3880,#2580,.T.);
#5038=EDGE_CURVE('',#3878,#3881,#1926,.T.);
#5039=EDGE_CURVE('',#3880,#3881,#2581,.T.);
#5040=EDGE_CURVE('',#3881,#3882,#2019,.T.);
#5041=EDGE_CURVE('',#3879,#3883,#1927,.F.);
#5042=EDGE_CURVE('',#3884,#3883,#279,.T.);
#5043=EDGE_CURVE('',#3882,#3884,#2582,.T.);
#5044=EDGE_CURVE('',#3882,#3885,#1928,.T.);
#5045=EDGE_CURVE('',#3885,#3884,#2583,.F.);
#5046=EDGE_CURVE('',#3885,#3886,#1929,.T.);
#5047=EDGE_CURVE('',#3883,#3887,#2584,.F.);
#5048=EDGE_CURVE('',#3888,#3887,#280,.F.);
#5049=EDGE_CURVE('',#3886,#3888,#2585,.T.);
#5050=EDGE_CURVE('',#3886,#3889,#1930,.T.);
#5051=EDGE_CURVE('',#3888,#3889,#2586,.T.);
#5052=EDGE_CURVE('',#3890,#3891,#2020,.T.);
#5053=EDGE_CURVE('',#3892,#3890,#2587,.T.);
#5054=EDGE_CURVE('',#3892,#3893,#281,.F.);
#5055=EDGE_CURVE('',#3893,#3894,#1931,.F.);
#5056=EDGE_CURVE('',#3895,#3894,#282,.T.);
#5057=EDGE_CURVE('',#3891,#3895,#2588,.T.);
#5058=EDGE_CURVE('',#3891,#3896,#1932,.T.);
#5059=EDGE_CURVE('',#3896,#3895,#2589,.F.);
#5060=EDGE_CURVE('',#3889,#3897,#2021,.T.);
#5061=EDGE_CURVE('',#3887,#3898,#1933,.F.);
#5062=EDGE_CURVE('',#3899,#3898,#283,.T.);
#5063=EDGE_CURVE('',#3897,#3899,#2590,.T.);
#5064=EDGE_CURVE('',#3897,#3900,#1934,.T.);
#5065=EDGE_CURVE('',#3900,#3899,#2591,.F.);
#5066=EDGE_CURVE('',#3901,#3871,#1935,.T.);
#5067=EDGE_CURVE('',#3901,#3873,#2592,.T.);
#5068=EDGE_CURVE('',#3896,#3902,#1936,.T.);
#5069=EDGE_CURVE('',#3894,#3874,#2593,.F.);
#5070=EDGE_CURVE('',#3902,#3901,#1937,.T.);
#5071=EDGE_CURVE('',#3903,#3890,#1938,.T.);
#5072=EDGE_CURVE('',#3903,#3892,#2594,.T.);
#5073=EDGE_CURVE('',#3900,#3903,#1939,.T.);
#5074=EDGE_CURVE('',#3898,#3893,#2595,.F.);
#5075=EDGE_CURVE('',#3904,#3904,#1940,.T.);
#5076=EDGE_CURVE('',#3904,#3905,#1941,.T.);
#5077=EDGE_CURVE('',#3905,#3905,#1942,.T.);
#5078=EDGE_CURVE('',#3906,#3906,#1943,.T.);
#5079=EDGE_CURVE('',#3907,#3907,#1944,.T.);
#5080=EDGE_CURVE('',#3907,#3905,#2596,.T.);
#5081=EDGE_CURVE('',#3908,#3908,#1945,.T.);
#5082=EDGE_CURVE('',#3908,#3907,#2597,.T.);
#5083=EDGE_CURVE('',#3909,#3909,#1946,.F.);
#5084=EDGE_CURVE('',#3909,#3908,#2598,.T.);
#5085=EDGE_CURVE('',#3902,#3910,#1947,.T.);
#5086=EDGE_CURVE('',#3911,#3910,#1948,.T.);
#5087=EDGE_CURVE('',#3910,#3911,#1949,.T.);
#5088=EDGE_CURVE('',#3906,#3911,#2599,.T.);
#7317=ORIENTED_EDGE('',*,*,#5026,.F.);
#7318=ORIENTED_EDGE('',*,*,#5027,.F.);
#7319=ORIENTED_EDGE('',*,*,#5028,.T.);
#7320=ORIENTED_EDGE('',*,*,#5029,.T.);
#7321=ORIENTED_EDGE('',*,*,#5030,.F.);
#7322=ORIENTED_EDGE('',*,*,#5031,.F.);
#7323=ORIENTED_EDGE('',*,*,#5032,.F.);
#7324=ORIENTED_EDGE('',*,*,#5031,.T.);
#7325=ORIENTED_EDGE('',*,*,#5033,.F.);
#7326=ORIENTED_EDGE('',*,*,#5034,.F.);
#7327=ORIENTED_EDGE('',*,*,#5033,.T.);
#7328=ORIENTED_EDGE('',*,*,#5030,.T.);
#7329=ORIENTED_EDGE('',*,*,#5035,.T.);
#7330=ORIENTED_EDGE('',*,*,#5036,.F.);
#7331=ORIENTED_EDGE('',*,*,#5037,.F.);
#7332=ORIENTED_EDGE('',*,*,#5038,.F.);
#7333=ORIENTED_EDGE('',*,*,#5037,.T.);
#7334=ORIENTED_EDGE('',*,*,#5039,.T.);
#7335=ORIENTED_EDGE('',*,*,#5040,.F.);
#7336=ORIENTED_EDGE('',*,*,#5039,.F.);
#7337=ORIENTED_EDGE('',*,*,#5036,.T.);
#7338=ORIENTED_EDGE('',*,*,#5041,.T.);
#7339=ORIENTED_EDGE('',*,*,#5042,.F.);
#7340=ORIENTED_EDGE('',*,*,#5043,.F.);
#7341=ORIENTED_EDGE('',*,*,#5044,.F.);
#7342=ORIENTED_EDGE('',*,*,#5043,.T.);
#7343=ORIENTED_EDGE('',*,*,#5045,.F.);
#7344=ORIENTED_EDGE('',*,*,#5046,.F.);
#7345=ORIENTED_EDGE('',*,*,#5045,.T.);
#7346=ORIENTED_EDGE('',*,*,#5042,.T.);
#7347=ORIENTED_EDGE('',*,*,#5047,.T.);
#7348=ORIENTED_EDGE('',*,*,#5048,.F.);
#7349=ORIENTED_EDGE('',*,*,#5049,.F.);
#7350=ORIENTED_EDGE('',*,*,#5050,.F.);
#7351=ORIENTED_EDGE('',*,*,#5049,.T.);
#7352=ORIENTED_EDGE('',*,*,#5051,.T.);
#7353=ORIENTED_EDGE('',*,*,#5052,.F.);
#7354=ORIENTED_EDGE('',*,*,#5053,.F.);
#7355=ORIENTED_EDGE('',*,*,#5054,.T.);
#7356=ORIENTED_EDGE('',*,*,#5055,.T.);
#7357=ORIENTED_EDGE('',*,*,#5056,.F.);
#7358=ORIENTED_EDGE('',*,*,#5057,.F.);
#7359=ORIENTED_EDGE('',*,*,#5058,.F.);
#7360=ORIENTED_EDGE('',*,*,#5057,.T.);
#7361=ORIENTED_EDGE('',*,*,#5059,.F.);
#7362=ORIENTED_EDGE('',*,*,#5060,.F.);
#7363=ORIENTED_EDGE('',*,*,#5051,.F.);
#7364=ORIENTED_EDGE('',*,*,#5048,.T.);
#7365=ORIENTED_EDGE('',*,*,#5061,.T.);
#7366=ORIENTED_EDGE('',*,*,#5062,.F.);
#7367=ORIENTED_EDGE('',*,*,#5063,.F.);
#7368=ORIENTED_EDGE('',*,*,#5064,.F.);
#7369=ORIENTED_EDGE('',*,*,#5063,.T.);
#7370=ORIENTED_EDGE('',*,*,#5065,.F.);
#7371=ORIENTED_EDGE('',*,*,#5066,.F.);
#7372=ORIENTED_EDGE('',*,*,#5067,.T.);
#7373=ORIENTED_EDGE('',*,*,#5027,.T.);
#7374=ORIENTED_EDGE('',*,*,#5068,.F.);
#7375=ORIENTED_EDGE('',*,*,#5059,.T.);
#7376=ORIENTED_EDGE('',*,*,#5056,.T.);
#7377=ORIENTED_EDGE('',*,*,#5069,.T.);
#7378=ORIENTED_EDGE('',*,*,#5028,.F.);
#7379=ORIENTED_EDGE('',*,*,#5067,.F.);
#7380=ORIENTED_EDGE('',*,*,#5070,.F.);
#7381=ORIENTED_EDGE('',*,*,#5071,.F.);
#7382=ORIENTED_EDGE('',*,*,#5072,.T.);
#7383=ORIENTED_EDGE('',*,*,#5053,.T.);
#7384=ORIENTED_EDGE('',*,*,#5073,.F.);
#7385=ORIENTED_EDGE('',*,*,#5065,.T.);
#7386=ORIENTED_EDGE('',*,*,#5062,.T.);
#7387=ORIENTED_EDGE('',*,*,#5074,.T.);
#7388=ORIENTED_EDGE('',*,*,#5054,.F.);
#7389=ORIENTED_EDGE('',*,*,#5072,.F.);
#7390=ORIENTED_EDGE('',*,*,#5035,.F.);
#7391=ORIENTED_EDGE('',*,*,#5029,.F.);
#7392=ORIENTED_EDGE('',*,*,#5069,.F.);
#7393=ORIENTED_EDGE('',*,*,#5055,.F.);
#7394=ORIENTED_EDGE('',*,*,#5074,.F.);
#7395=ORIENTED_EDGE('',*,*,#5061,.F.);
#7396=ORIENTED_EDGE('',*,*,#5047,.F.);
#7397=ORIENTED_EDGE('',*,*,#5041,.F.);
#7398=ORIENTED_EDGE('',*,*,#5075,.T.);
#7399=ORIENTED_EDGE('',*,*,#5076,.T.);
#7400=ORIENTED_EDGE('',*,*,#5077,.T.);
#7401=ORIENTED_EDGE('',*,*,#5076,.F.);
#7402=ORIENTED_EDGE('',*,*,#5078,.T.);
#7403=ORIENTED_EDGE('',*,*,#5075,.F.);
#7404=ORIENTED_EDGE('',*,*,#5079,.F.);
#7405=ORIENTED_EDGE('',*,*,#5080,.T.);
#7406=ORIENTED_EDGE('',*,*,#5077,.F.);
#7407=ORIENTED_EDGE('',*,*,#5080,.F.);
#7408=ORIENTED_EDGE('',*,*,#5081,.F.);
#7409=ORIENTED_EDGE('',*,*,#5082,.T.);
#7410=ORIENTED_EDGE('',*,*,#5079,.T.);
#7411=ORIENTED_EDGE('',*,*,#5082,.F.);
#7412=ORIENTED_EDGE('',*,*,#5083,.F.);
#7413=ORIENTED_EDGE('',*,*,#5084,.T.);
#7414=ORIENTED_EDGE('',*,*,#5081,.T.);
#7415=ORIENTED_EDGE('',*,*,#5084,.F.);
#7416=ORIENTED_EDGE('',*,*,#5083,.T.);
#7417=ORIENTED_EDGE('',*,*,#5060,.T.);
#7418=ORIENTED_EDGE('',*,*,#5064,.T.);
#7419=ORIENTED_EDGE('',*,*,#5073,.T.);
#7420=ORIENTED_EDGE('',*,*,#5071,.T.);
#7421=ORIENTED_EDGE('',*,*,#5052,.T.);
#7422=ORIENTED_EDGE('',*,*,#5058,.T.);
#7423=ORIENTED_EDGE('',*,*,#5068,.T.);
#7424=ORIENTED_EDGE('',*,*,#5085,.T.);
#7425=ORIENTED_EDGE('',*,*,#5086,.F.);
#7426=ORIENTED_EDGE('',*,*,#5087,.F.);
#7427=ORIENTED_EDGE('',*,*,#5085,.F.);
#7428=ORIENTED_EDGE('',*,*,#5070,.T.);
#7429=ORIENTED_EDGE('',*,*,#5066,.T.);
#7430=ORIENTED_EDGE('',*,*,#5026,.T.);
#7431=ORIENTED_EDGE('',*,*,#5032,.T.);
#7432=ORIENTED_EDGE('',*,*,#5034,.T.);
#7433=ORIENTED_EDGE('',*,*,#5038,.T.);
#7434=ORIENTED_EDGE('',*,*,#5040,.T.);
#7435=ORIENTED_EDGE('',*,*,#5044,.T.);
#7436=ORIENTED_EDGE('',*,*,#5046,.T.);
#7437=ORIENTED_EDGE('',*,*,#5050,.T.);
#7438=ORIENTED_EDGE('',*,*,#5078,.F.);
#7439=ORIENTED_EDGE('',*,*,#5088,.T.);
#7440=ORIENTED_EDGE('',*,*,#5086,.T.);
#7441=ORIENTED_EDGE('',*,*,#5087,.T.);
#7442=ORIENTED_EDGE('',*,*,#5088,.F.);
#7632=CYLINDRICAL_SURFACE('',#9179,0.496);
#7633=CYLINDRICAL_SURFACE('',#9190,0.496);
#7634=CYLINDRICAL_SURFACE('',#9200,0.496);
#7635=CYLINDRICAL_SURFACE('',#9206,0.496);
#7636=CYLINDRICAL_SURFACE('',#9227,0.839230484541328);
#7637=CYLINDRICAL_SURFACE('',#9231,0.96675);
#8090=ADVANCED_FACE('',(#928),#7632,.T.);
#8091=ADVANCED_FACE('',(#929),#461,.F.);
#8092=ADVANCED_FACE('',(#930),#462,.F.);
#8093=ADVANCED_FACE('',(#931),#463,.F.);
#8094=ADVANCED_FACE('',(#932),#7633,.T.);
#8095=ADVANCED_FACE('',(#933),#464,.F.);
#8096=ADVANCED_FACE('',(#934),#465,.F.);
#8097=ADVANCED_FACE('',(#935),#466,.F.);
#8098=ADVANCED_FACE('',(#936),#7634,.T.);
#8099=ADVANCED_FACE('',(#937),#467,.F.);
#8100=ADVANCED_FACE('',(#938),#7635,.T.);
#8101=ADVANCED_FACE('',(#939),#468,.F.);
#8102=ADVANCED_FACE('',(#940),#469,.F.);
#8103=ADVANCED_FACE('',(#941),#470,.F.);
#8104=ADVANCED_FACE('',(#942),#471,.F.);
#8105=ADVANCED_FACE('',(#943),#472,.F.);
#8106=ADVANCED_FACE('',(#944),#473,.F.);
#8107=ADVANCED_FACE('',(#945),#236,.F.);
#8108=ADVANCED_FACE('',(#946,#177),#474,.T.);
#8109=ADVANCED_FACE('',(#947),#7636,.T.);
#8110=ADVANCED_FACE('',(#948),#68,.T.);
#8111=ADVANCED_FACE('',(#949),#7637,.T.);
#8112=ADVANCED_FACE('',(#950),#475,.T.);
#8113=ADVANCED_FACE('',(#951),#213,.T.);
#8114=ADVANCED_FACE('',(#952),#69,.T.);
#8126=CLOSED_SHELL('',(#8090,#8091,#8092,#8093,#8094,#8095,#8096,#8097,
#8098,#8099,#8100,#8101,#8102,#8103,#8104,#8105,#8106,#8107,#8108,#8109,
#8110,#8111,#8112,#8113,#8114));
#9178=AXIS2_PLACEMENT_3D('',#16817,#11641,#11642);
#9179=AXIS2_PLACEMENT_3D('',#16818,#11643,#11644);
#9180=AXIS2_PLACEMENT_3D('',#16839,#11646,#11647);
#9181=AXIS2_PLACEMENT_3D('',#16841,#11648,#11649);
#9182=AXIS2_PLACEMENT_3D('',#16843,#11650,#11651);
#9183=AXIS2_PLACEMENT_3D('',#16845,#11653,#11654);
#9184=AXIS2_PLACEMENT_3D('',#16847,#11655,#11656);
#9185=AXIS2_PLACEMENT_3D('',#16849,#11658,#11659);
#9186=AXIS2_PLACEMENT_3D('',#16851,#11660,#11661);
#9187=AXIS2_PLACEMENT_3D('',#16855,#11663,#11664);
#9188=AXIS2_PLACEMENT_3D('',#16857,#11666,#11667);
#9189=AXIS2_PLACEMENT_3D('',#16859,#11668,#11669);
#9190=AXIS2_PLACEMENT_3D('',#16861,#11671,#11672);
#9191=AXIS2_PLACEMENT_3D('',#16879,#11673,#11674);
#9192=AXIS2_PLACEMENT_3D('',#16881,#11675,#11676);
#9193=AXIS2_PLACEMENT_3D('',#16883,#11678,#11679);
#9194=AXIS2_PLACEMENT_3D('',#16885,#11680,#11681);
#9195=AXIS2_PLACEMENT_3D('',#16887,#11683,#11684);
#9196=AXIS2_PLACEMENT_3D('',#16889,#11685,#11686);
#9197=AXIS2_PLACEMENT_3D('',#16893,#11688,#11689);
#9198=AXIS2_PLACEMENT_3D('',#16895,#11691,#11692);
#9199=AXIS2_PLACEMENT_3D('',#16897,#11693,#11694);
#9200=AXIS2_PLACEMENT_3D('',#16899,#11696,#11697);
#9201=AXIS2_PLACEMENT_3D('',#16920,#11699,#11700);
#9202=AXIS2_PLACEMENT_3D('',#16922,#11701,#11702);
#9203=AXIS2_PLACEMENT_3D('',#16924,#11703,#11704);
#9204=AXIS2_PLACEMENT_3D('',#16926,#11706,#11707);
#9205=AXIS2_PLACEMENT_3D('',#16928,#11708,#11709);
#9206=AXIS2_PLACEMENT_3D('',#16930,#11711,#11712);
#9207=AXIS2_PLACEMENT_3D('',#16948,#11713,#11714);
#9208=AXIS2_PLACEMENT_3D('',#16950,#11715,#11716);
#9209=AXIS2_PLACEMENT_3D('',#16952,#11718,#11719);
#9210=AXIS2_PLACEMENT_3D('',#16954,#11720,#11721);
#9211=AXIS2_PLACEMENT_3D('',#16956,#11723,#11724);
#9212=AXIS2_PLACEMENT_3D('',#16958,#11725,#11726);
#9213=AXIS2_PLACEMENT_3D('',#16960,#11728,#11729);
#9214=AXIS2_PLACEMENT_3D('',#16962,#11730,#11731);
#9215=AXIS2_PLACEMENT_3D('',#16964,#11733,#11734);
#9216=AXIS2_PLACEMENT_3D('',#16965,#11735,#11736);
#9217=AXIS2_PLACEMENT_3D('',#16967,#11737,#11738);
#9218=AXIS2_PLACEMENT_3D('',#16969,#11740,#11741);
#9219=AXIS2_PLACEMENT_3D('',#16970,#11742,#11743);
#9220=AXIS2_PLACEMENT_3D('',#16972,#11745,#11746);
#9221=AXIS2_PLACEMENT_3D('',#16973,#11747,#11748);
#9222=AXIS2_PLACEMENT_3D('',#16975,#11749,#11750);
#9223=AXIS2_PLACEMENT_3D('',#16977,#11751,#11752);
#9224=AXIS2_PLACEMENT_3D('',#16978,#11753,#11754);
#9225=AXIS2_PLACEMENT_3D('',#16979,#11755,#11756);
#9226=AXIS2_PLACEMENT_3D('',#16981,#11757,#11758);
#9227=AXIS2_PLACEMENT_3D('',#16982,#11759,#11760);
#9228=AXIS2_PLACEMENT_3D('',#16984,#11761,#11762);
#9229=AXIS2_PLACEMENT_3D('',#16986,#11764,#11765);
#9230=AXIS2_PLACEMENT_3D('',#16988,#11766,#11767);
#9231=AXIS2_PLACEMENT_3D('',#16990,#11769,#11770);
#9232=AXIS2_PLACEMENT_3D('',#16992,#11771,#11772);
#9233=AXIS2_PLACEMENT_3D('',#16994,#11774,#11775);
#9234=AXIS2_PLACEMENT_3D('',#16995,#11776,#11777);
#9235=AXIS2_PLACEMENT_3D('',#16997,#11778,#11779);
#9236=AXIS2_PLACEMENT_3D('',#16999,#11780,#11781);
#9237=AXIS2_PLACEMENT_3D('',#17000,#11782,#11783);
#9238=AXIS2_PLACEMENT_3D('',#17001,#11784,#11785);
#11641=DIRECTION('axis',(0.,0.,1.));
#11642=DIRECTION('refdir',(1.,0.,0.));
#11643=DIRECTION('center_axis',(0.,0.,-1.));
#11644=DIRECTION('ref_axis',(0.707106781186864,-0.707106781186231,0.));
#11645=DIRECTION('',(0.,0.,1.));
#11646=DIRECTION('center_axis',(-0.866025403784439,2.42308806056559E-16,
-0.5));
#11647=DIRECTION('ref_axis',(0.5,-1.39897054514259E-16,-0.866025403784439));
#11648=DIRECTION('center_axis',(0.,0.,-1.));
#11649=DIRECTION('ref_axis',(0.707106781186864,-0.707106781186231,0.));
#11650=DIRECTION('center_axis',(-1.34432925600244E-12,0.866025403784439,
-0.5));
#11651=DIRECTION('ref_axis',(7.76183832708735E-13,-0.5,-0.866025403784439));
#11652=DIRECTION('',(0.,0.,-1.));
#11653=DIRECTION('center_axis',(-1.,-8.96558844583498E-13,0.));
#11654=DIRECTION('ref_axis',(-8.96558844583498E-13,1.,0.));
#11655=DIRECTION('center_axis',(-1.,-8.96558844583498E-13,0.));
#11656=DIRECTION('ref_axis',(0.,0.,-1.));
#11657=DIRECTION('',(-4.48279422291749E-13,0.5,0.866025403784439));
#11658=DIRECTION('center_axis',(-1.34432925600244E-12,0.866025403784439,
-0.5));
#11659=DIRECTION('ref_axis',(1.,1.55229771566499E-12,0.));
#11660=DIRECTION('center_axis',(-1.34432925600244E-12,0.866025403784439,
-0.5));
#11661=DIRECTION('ref_axis',(0.,-0.5,-0.866025403784439));
#11662=DIRECTION('',(-1.,-1.55229771566499E-12,0.));
#11663=DIRECTION('center_axis',(-1.34432925600244E-12,0.866025403784439,
-0.5));
#11664=DIRECTION('ref_axis',(7.76183832708735E-13,-0.5,-0.866025403784439));
#11665=DIRECTION('',(7.28095205575773E-14,-0.5,-0.866025403784439));
#11666=DIRECTION('center_axis',(1.,1.45619041115155E-13,0.));
#11667=DIRECTION('ref_axis',(1.45619041115155E-13,-1.,0.));
#11668=DIRECTION('center_axis',(1.,1.45619041115155E-13,0.));
#11669=DIRECTION('ref_axis',(0.,0.,1.));
#11670=DIRECTION('',(0.,0.,1.));
#11671=DIRECTION('center_axis',(0.,0.,-1.));
#11672=DIRECTION('ref_axis',(-0.707106781186035,-0.70710678118706,0.));
#11673=DIRECTION('center_axis',(0.,0.,-1.));
#11674=DIRECTION('ref_axis',(-0.707106781186035,-0.70710678118706,0.));
#11675=DIRECTION('center_axis',(0.866025403784439,1.82700839766916E-13,
-0.5));
#11676=DIRECTION('ref_axis',(-0.5,-1.0551735336738E-13,-0.866025403784439));
#11677=DIRECTION('',(0.,0.,-1.));
#11678=DIRECTION('center_axis',(-1.30466679482154E-12,1.,0.));
#11679=DIRECTION('ref_axis',(1.,1.30466679482154E-12,0.));
#11680=DIRECTION('center_axis',(-1.30466679482154E-12,1.,0.));
#11681=DIRECTION('ref_axis',(0.,0.,-1.));
#11682=DIRECTION('',(0.5,6.52333397410772E-13,0.866025403784439));
#11683=DIRECTION('center_axis',(0.866025403784439,1.82700839766916E-13,
-0.5));
#11684=DIRECTION('ref_axis',(2.10964758041199E-13,-1.,0.));
#11685=DIRECTION('center_axis',(0.866025403784439,1.82700839766916E-13,
-0.5));
#11686=DIRECTION('ref_axis',(0.5,0.,0.866025403784439));
#11687=DIRECTION('',(-2.10964758041199E-13,1.,0.));
#11688=DIRECTION('center_axis',(0.866025403784439,1.82700839766916E-13,
-0.5));
#11689=DIRECTION('ref_axis',(-0.5,-1.05482379103751E-13,-0.866025403784439));
#11690=DIRECTION('',(-0.5,6.4832235838889E-13,-0.866025403784439));
#11691=DIRECTION('center_axis',(-1.29664471677778E-12,-1.,0.));
#11692=DIRECTION('ref_axis',(-1.,1.29664471677778E-12,0.));
#11693=DIRECTION('center_axis',(-1.29664471677778E-12,-1.,0.));
#11694=DIRECTION('ref_axis',(0.,0.,1.));
#11695=DIRECTION('',(0.,0.,1.));
#11696=DIRECTION('center_axis',(0.,0.,-1.));
#11697=DIRECTION('ref_axis',(0.707106781186895,0.7071067811862,0.));
#11698=DIRECTION('',(0.,0.,1.));
#11699=DIRECTION('center_axis',(-1.35644469630397E-12,-0.866025403784439,
-0.5));
#11700=DIRECTION('ref_axis',(7.8314371117082E-13,0.5,-0.866025403784439));
#11701=DIRECTION('center_axis',(0.,0.,-1.));
#11702=DIRECTION('ref_axis',(0.707106781186895,0.7071067811862,0.));
#11703=DIRECTION('center_axis',(-0.866025403784439,2.42308806056559E-16,
-0.5));
#11704=DIRECTION('ref_axis',(0.5,-1.39897054514259E-16,-0.866025403784439));
#11705=DIRECTION('',(0.,0.,-1.));
#11706=DIRECTION('center_axis',(1.80920256647203E-12,-1.,0.));
#11707=DIRECTION('ref_axis',(-1.,-1.80920256647203E-12,0.));
#11708=DIRECTION('center_axis',(1.80920256647203E-12,-1.,0.));
#11709=DIRECTION('ref_axis',(0.,0.,1.));
#11710=DIRECTION('',(-0.5,-9.04601283236015E-13,0.866025403784439));
#11711=DIRECTION('center_axis',(0.,0.,-1.));
#11712=DIRECTION('ref_axis',(-0.707106781186768,0.707106781186327,0.));
#11713=DIRECTION('center_axis',(0.,0.,-1.));
#11714=DIRECTION('ref_axis',(-0.707106781186768,0.707106781186327,0.));
#11715=DIRECTION('center_axis',(-1.35644469630397E-12,-0.866025403784439,
-0.5));
#11716=DIRECTION('ref_axis',(7.83108736907191E-13,0.5,-0.866025403784439));
#11717=DIRECTION('',(0.,0.,-1.));
#11718=DIRECTION('center_axis',(1.,1.91935343509834E-12,0.));
#11719=DIRECTION('ref_axis',(1.91935343509834E-12,-1.,0.));
#11720=DIRECTION('center_axis',(1.,1.91935343509834E-12,0.));
#11721=DIRECTION('ref_axis',(0.,0.,1.));
#11722=DIRECTION('',(9.59676717549172E-13,-0.5,0.866025403784439));
#11723=DIRECTION('center_axis',(-1.62884833462111E-16,1.,0.));
#11724=DIRECTION('ref_axis',(1.,1.62884833462111E-16,0.));
#11725=DIRECTION('center_axis',(-1.62884833462111E-16,1.,0.));
#11726=DIRECTION('ref_axis',(0.,0.,-1.));
#11727=DIRECTION('',(0.5,8.14424167310554E-17,-0.866025403784439));
#11728=DIRECTION('center_axis',(-0.866025403784439,2.42308806056559E-16,
-0.5));
#11729=DIRECTION('ref_axis',(2.79794108807543E-16,1.,0.));
#11730=DIRECTION('center_axis',(-0.866025403784439,2.42308806056559E-16,
-0.5));
#11731=DIRECTION('ref_axis',(0.5,0.,-0.866025403784439));
#11732=DIRECTION('',(-2.79794108807543E-16,-1.,0.));
#11733=DIRECTION('center_axis',(-0.866025403784439,2.42308806056559E-16,
-0.5));
#11734=DIRECTION('ref_axis',(0.5,0.,-0.866025403784439));
#11735=DIRECTION('center_axis',(-1.,2.79168316070879E-12,0.));
#11736=DIRECTION('ref_axis',(2.79168316070879E-12,1.,0.));
#11737=DIRECTION('center_axis',(-1.,2.79168316070879E-12,0.));
#11738=DIRECTION('ref_axis',(0.,0.,-1.));
#11739=DIRECTION('',(1.3958415803544E-12,0.5,-0.866025403784439));
#11740=DIRECTION('center_axis',(-1.35644469630397E-12,-0.866025403784439,
-0.5));
#11741=DIRECTION('ref_axis',(-1.,1.56628742110387E-12,0.));
#11742=DIRECTION('center_axis',(-1.35644469630397E-12,-0.866025403784439,
-0.5));
#11743=DIRECTION('ref_axis',(0.,-0.5,0.866025403784439));
#11744=DIRECTION('',(1.,-1.56628742110387E-12,0.));
#11745=DIRECTION('center_axis',(0.,0.,-1.));
#11746=DIRECTION('ref_axis',(-1.,0.,0.));
#11747=DIRECTION('center_axis',(0.,0.,-1.));
#11748=DIRECTION('ref_axis',(-1.,0.,0.));
#11749=DIRECTION('center_axis',(0.,0.,-1.));
#11750=DIRECTION('ref_axis',(1.,0.,0.));
#11751=DIRECTION('center_axis',(-1.22464679914735E-16,-1.,0.));
#11752=DIRECTION('ref_axis',(1.,-1.22464679914735E-16,0.));
#11753=DIRECTION('center_axis',(0.,0.,1.));
#11754=DIRECTION('ref_axis',(1.,0.,0.));
#11755=DIRECTION('center_axis',(0.,0.,-1.));
#11756=DIRECTION('ref_axis',(-1.,0.,0.));
#11757=DIRECTION('center_axis',(0.,0.,-1.));
#11758=DIRECTION('ref_axis',(1.,0.,0.));
#11759=DIRECTION('center_axis',(0.,0.,-1.));
#11760=DIRECTION('ref_axis',(-1.,0.,0.));
#11761=DIRECTION('center_axis',(0.,0.,-1.));
#11762=DIRECTION('ref_axis',(1.,0.,0.));
#11763=DIRECTION('',(0.,0.,1.));
#11764=DIRECTION('center_axis',(0.,0.,-1.));
#11765=DIRECTION('ref_axis',(-1.,0.,0.));
#11766=DIRECTION('center_axis',(0.,0.,-1.));
#11767=DIRECTION('ref_axis',(-1.,0.,0.));
#11768=DIRECTION('',(-0.258819045102519,3.16961915143174E-17,0.965925826289069));
#11769=DIRECTION('center_axis',(0.,0.,-1.));
#11770=DIRECTION('ref_axis',(-1.,0.,0.));
#11771=DIRECTION('center_axis',(0.,0.,1.));
#11772=DIRECTION('ref_axis',(-1.,0.,0.));
#11773=DIRECTION('',(0.,0.,1.));
#11774=DIRECTION('center_axis',(0.,0.,-1.));
#11775=DIRECTION('ref_axis',(-1.,0.,0.));
#11776=DIRECTION('center_axis',(6.12323399573676E-17,0.,1.));
#11777=DIRECTION('ref_axis',(1.,0.,0.));
#11778=DIRECTION('center_axis',(1.22464679914735E-16,-1.,0.));
#11779=DIRECTION('ref_axis',(-1.,-1.22464679914735E-16,0.));
#11780=DIRECTION('center_axis',(0.,0.,-1.));
#11781=DIRECTION('ref_axis',(1.,0.,0.));
#11782=DIRECTION('center_axis',(0.,0.,-1.));
#11783=DIRECTION('ref_axis',(1.,0.,0.));
#11784=DIRECTION('center_axis',(0.,0.,-1.));
#11785=DIRECTION('ref_axis',(-1.,0.,0.));
#11786=DIRECTION('',(-0.087155742757872,1.06735001395738E-17,0.996194698090852));
#16817=CARTESIAN_POINT('',(0.,0.,0.));
#16818=CARTESIAN_POINT('Origin',(-0.744000000195138,0.744000000196221,1.2));
#16819=CARTESIAN_POINT('',(-0.744000000195138,0.248000000196221,1.15122809938326));
#16820=CARTESIAN_POINT('',(-0.248000000195138,0.744000000196666,1.15122809938313));
#16821=CARTESIAN_POINT('Ctrl Pts',(-0.744000000195138,0.248000000196221,
1.15122809938326));
#16822=CARTESIAN_POINT('Ctrl Pts',(-0.743548129195526,0.248000000196221,
1.15128162561029));
#16823=CARTESIAN_POINT('Ctrl Pts',(-0.743096462399636,0.248000617700407,
1.15133505381795));
#16824=CARTESIAN_POINT('Ctrl Pts',(-0.68084251616827,0.248170686680912,
1.1586889909138));
#16825=CARTESIAN_POINT('Ctrl Pts',(-0.614748859330863,0.260619583354249,
1.16502989619583));
#16826=CARTESIAN_POINT('Ctrl Pts',(-0.492966510303847,0.311166686726808,
1.17344391775669));
#16827=CARTESIAN_POINT('Ctrl Pts',(-0.437280006866291,0.349270066587974,
1.17551763482271));
#16828=CARTESIAN_POINT('Ctrl Pts',(-0.393275036726453,0.393275036727851,
1.17551763482269));
#16829=CARTESIAN_POINT('Ctrl Pts',(-0.349270066586615,0.437280006867729,
1.17551763482268));
#16830=CARTESIAN_POINT('Ctrl Pts',(-0.3111666867255,0.49296651030532,1.17344391775664));
#16831=CARTESIAN_POINT('Ctrl Pts',(-0.26061958335305,0.61474885933238,1.16502989619573));
#16832=CARTESIAN_POINT('Ctrl Pts',(-0.248170686679772,0.680842516169798,
1.15868899091368));
#16833=CARTESIAN_POINT('Ctrl Pts',(-0.248000617699323,0.743096462401038,
1.15133505381783));
#16834=CARTESIAN_POINT('Ctrl Pts',(-0.248000000195138,0.743548129196929,
1.15128162561017));
#16835=CARTESIAN_POINT('Ctrl Pts',(-0.248000000195138,0.744000000196666,
1.15122809938313));
#16836=CARTESIAN_POINT('',(-0.744000000195138,0.248000000196221,0.583389912843141));
#16837=CARTESIAN_POINT('',(-0.744000000195138,0.248000000196221,1.2));
#16838=CARTESIAN_POINT('',(-0.516876228118667,0.303056928861888,0.19));
#16839=CARTESIAN_POINT('Origin',(-0.744000000195138,0.744000000196221,0.583389912843142));
#16840=CARTESIAN_POINT('',(-0.303056928861701,0.51687622811801,0.19));
#16841=CARTESIAN_POINT('Origin',(-0.744000000195138,0.744000000196221,0.19));
#16842=CARTESIAN_POINT('',(-0.248000000195138,0.744000000196666,0.583389912846777));
#16843=CARTESIAN_POINT('Origin',(-0.744000000195138,0.744000000196221,0.583389912847341));
#16844=CARTESIAN_POINT('',(-0.248000000195138,0.744000000196666,1.2));
#16845=CARTESIAN_POINT('Origin',(-0.248000000194694,0.24800000019315,1.2));
#16846=CARTESIAN_POINT('',(-0.24800000019541,1.04682989872245,1.10790668314437));
#16847=CARTESIAN_POINT('Origin',(-0.248000000194471,-2.22346593631069E-13,
-5.12965591734105));
#16848=CARTESIAN_POINT('',(-0.248000000195362,0.993500000023809,1.01553658903582));
#16849=CARTESIAN_POINT('Origin',(-0.248000000195457,1.09999999999962,1.2));
#16850=CARTESIAN_POINT('',(0.248000000196041,1.04682989872314,1.10790668314423));
#16851=CARTESIAN_POINT('Origin',(2.9811416492917E-12,-1.91582141081592,
-4.02355591008723));
#16852=CARTESIAN_POINT('',(0.303056928861511,0.516876228118951,0.19));
#16853=CARTESIAN_POINT('',(-0.124000000097707,0.516876228118288,0.19));
#16854=CARTESIAN_POINT('',(0.248000000196085,0.744000000194883,0.583389912842355));
#16855=CARTESIAN_POINT('Origin',(0.744000000196085,0.744000000194955,0.583389912841147));
#16856=CARTESIAN_POINT('',(0.248000000196033,1.1000000000003,1.19999999999985));
#16857=CARTESIAN_POINT('Origin',(0.248000000196033,1.10000000000039,1.2));
#16858=CARTESIAN_POINT('',(0.248000000196085,0.744000000194883,1.1512280993833));
#16859=CARTESIAN_POINT('Origin',(0.248000000196193,3.61135222251268E-14,
-5.12965591734105));
#16860=CARTESIAN_POINT('',(0.248000000196085,0.744000000194883,1.2));
#16861=CARTESIAN_POINT('Origin',(0.744000000196085,0.744000000194955,1.2));
#16862=CARTESIAN_POINT('',(0.744000000196732,0.248000000194955,1.15122809938313));
#16863=CARTESIAN_POINT('Ctrl Pts',(0.248000000196085,0.744000000194883,
1.1512280993833));
#16864=CARTESIAN_POINT('Ctrl Pts',(0.248000000196085,0.743548129195249,
1.15128162561033));
#16865=CARTESIAN_POINT('Ctrl Pts',(0.24800061770027,0.743096462399337,1.15133505381799));
#16866=CARTESIAN_POINT('Ctrl Pts',(0.248170686680793,0.68084251616795,1.15868899091384));
#16867=CARTESIAN_POINT('Ctrl Pts',(0.260619583354148,0.614748859330546,
1.16502989619587));
#16868=CARTESIAN_POINT('Ctrl Pts',(0.311166686726741,0.492966510303544,
1.17344391775672));
#16869=CARTESIAN_POINT('Ctrl Pts',(0.349270066587923,0.437280006865998,
1.17551763482273));
#16870=CARTESIAN_POINT('Ctrl Pts',(0.393275036727812,0.393275036726173,
1.17551763482271));
#16871=CARTESIAN_POINT('Ctrl Pts',(0.437280006867702,0.349270066586347,
1.1755176348227));
#16872=CARTESIAN_POINT('Ctrl Pts',(0.492966510305304,0.311166686725247,
1.17344391775665));
#16873=CARTESIAN_POINT('Ctrl Pts',(0.614748859332378,0.26061958335283,1.16502989619575));
#16874=CARTESIAN_POINT('Ctrl Pts',(0.6808425161698,0.248170686679572,1.15868899091369));
#16875=CARTESIAN_POINT('Ctrl Pts',(0.743096462401062,0.24800061769914,1.15133505381783));
#16876=CARTESIAN_POINT('Ctrl Pts',(0.743548129196974,0.248000000194955,
1.15128162561017));
#16877=CARTESIAN_POINT('Ctrl Pts',(0.744000000196732,0.248000000194955,
1.15122809938313));
#16878=CARTESIAN_POINT('',(0.516876228118432,0.30305692886123,0.19));
#16879=CARTESIAN_POINT('Origin',(0.744000000196085,0.744000000194955,0.19));
#16880=CARTESIAN_POINT('',(0.744000000196732,0.248000000194955,0.583389912846289));
#16881=CARTESIAN_POINT('Origin',(0.744000000196085,0.744000000194955,0.583389912845349));
#16882=CARTESIAN_POINT('',(0.744000000196732,0.248000000194955,1.2));
#16883=CARTESIAN_POINT('Origin',(0.248000000196157,0.248000000194308,1.2));
#16884=CARTESIAN_POINT('',(1.04682989872277,0.24800000019535,1.10790668314432));
#16885=CARTESIAN_POINT('Origin',(-3.16340915708764E-13,0.248000000193984,
-5.12965591734105));
#16886=CARTESIAN_POINT('',(0.99350000002449,0.248000000195281,1.01553658903639));
#16887=CARTESIAN_POINT('Origin',(1.09999999999997,0.248000000195419,1.2));
#16888=CARTESIAN_POINT('',(1.04682989872287,-0.248000000195507,1.1079066831443));
#16889=CARTESIAN_POINT('Origin',(-1.91582141081591,-4.04170800382928E-13,
-4.02355591008723));
#16890=CARTESIAN_POINT('',(0.51687622811856,-0.3030569288607,0.19));
#16891=CARTESIAN_POINT('',(0.51687622811847,0.124000000097702,0.19));
#16892=CARTESIAN_POINT('',(0.744000000195517,-0.248000000195115,0.583389912844004));
#16893=CARTESIAN_POINT('Origin',(0.744000000194874,-0.744000000195115,0.583389912842708));
#16894=CARTESIAN_POINT('',(1.09999999999998,-0.248000000195576,1.19999999999984));
#16895=CARTESIAN_POINT('Origin',(1.10000000000007,-0.248000000195576,1.2));
#16896=CARTESIAN_POINT('',(0.744000000195517,-0.248000000195115,1.15122809938326));
#16897=CARTESIAN_POINT('Origin',(-3.14351440352569E-13,-0.24800000019415,
-5.12965591734105));
#16898=CARTESIAN_POINT('',(0.744000000195517,-0.248000000195115,1.2));
#16899=CARTESIAN_POINT('Origin',(-0.744000000195415,-0.744000000194864,
1.2));
#16900=CARTESIAN_POINT('',(-0.248000000195415,-0.744000000196249,1.15122809938316));
#16901=CARTESIAN_POINT('',(-0.744000000196312,-0.248000000194864,1.15122809938318));
#16902=CARTESIAN_POINT('Ctrl Pts',(-0.248000000195415,-0.744000000196249,
1.15122809938316));
#16903=CARTESIAN_POINT('Ctrl Pts',(-0.248000000195414,-0.74354812919633,
1.15128162561023));
#16904=CARTESIAN_POINT('Ctrl Pts',(-0.248000617699598,-0.743096462400134,
1.15133505381792));
#16905=CARTESIAN_POINT('Ctrl Pts',(-0.248170686680046,-0.680842516168463,
1.15868899091381));
#16906=CARTESIAN_POINT('Ctrl Pts',(-0.260619583353321,-0.614748859331044,
1.16502989619585));
#16907=CARTESIAN_POINT('Ctrl Pts',(-0.311166686725766,-0.49296651030398,
1.17344391775673));
#16908=CARTESIAN_POINT('Ctrl Pts',(-0.349270066586879,-0.437280006866388,
1.17551763482276));
#16909=CARTESIAN_POINT('Ctrl Pts',(-0.393275036726715,-0.393275036726509,
1.17551763482276));
#16910=CARTESIAN_POINT('Ctrl Pts',(-0.437280006866551,-0.349270066586629,
1.17551763482276));
#16911=CARTESIAN_POINT('Ctrl Pts',(-0.492966510304106,-0.311166686725461,
1.17344391775673));
#16912=CARTESIAN_POINT('Ctrl Pts',(-0.61474885933112,-0.260619583352896,
1.16502989619586));
#16913=CARTESIAN_POINT('Ctrl Pts',(-0.680842516168527,-0.248170686679557,
1.15868899091382));
#16914=CARTESIAN_POINT('Ctrl Pts',(-0.743096462400073,-0.248000617699049,
1.15133505381795));
#16915=CARTESIAN_POINT('Ctrl Pts',(-0.74354812919627,-0.248000000194863,
1.15128162561025));
#16916=CARTESIAN_POINT('Ctrl Pts',(-0.744000000196312,-0.248000000194864,
1.15122809938318));
#16917=CARTESIAN_POINT('',(-0.248000000195415,-0.744000000196249,0.58338991284606));
#16918=CARTESIAN_POINT('',(-0.248000000195415,-0.744000000196249,1.2));
#16919=CARTESIAN_POINT('',(-0.303056928861281,-0.516876228118006,0.19));
#16920=CARTESIAN_POINT('Origin',(-0.744000000195415,-0.744000000194864,
0.583389912845007));
#16921=CARTESIAN_POINT('',(-0.516876228118667,-0.303056928860673,0.19));
#16922=CARTESIAN_POINT('Origin',(-0.744000000195415,-0.744000000194864,
0.19));
#16923=CARTESIAN_POINT('',(-0.744000000196312,-0.248000000194864,0.583389912845176));
#16924=CARTESIAN_POINT('Origin',(-0.744000000195415,-0.744000000194864,
0.583389912843621));
#16925=CARTESIAN_POINT('',(-0.744000000196312,-0.248000000194864,1.2));
#16926=CARTESIAN_POINT('Origin',(-0.24800000019403,-0.248000000193966,1.2));
#16927=CARTESIAN_POINT('',(-1.04682989872298,-0.248000000195412,1.10790668314428));
#16928=CARTESIAN_POINT('Origin',(4.5589868649524E-13,-0.248000000193518,
-5.12965591734105));
#16929=CARTESIAN_POINT('',(-0.993500000024419,-0.248000000195315,1.01553658903588));
#16930=CARTESIAN_POINT('Origin',(0.744000000194874,-0.744000000195115,1.2));
#16931=CARTESIAN_POINT('',(0.248000000194874,-0.744000000196067,1.15122809938321));
#16932=CARTESIAN_POINT('Ctrl Pts',(0.744000000195517,-0.248000000195115,
1.15122809938326));
#16933=CARTESIAN_POINT('Ctrl Pts',(0.743548129195714,-0.248000000195114,
1.15128162561031));
#16934=CARTESIAN_POINT('Ctrl Pts',(0.743096462399633,-0.248000617699299,
1.15133505381799));
#16935=CARTESIAN_POINT('Ctrl Pts',(0.680842516168076,-0.248170686679796,
1.15868899091386));
#16936=CARTESIAN_POINT('Ctrl Pts',(0.614748859330666,-0.260619583353124,
1.1650298961959));
#16937=CARTESIAN_POINT('Ctrl Pts',(0.492966510303643,-0.311166686725667,
1.17344391775676));
#16938=CARTESIAN_POINT('Ctrl Pts',(0.437280006866081,-0.349270066586825,
1.17551763482279));
#16939=CARTESIAN_POINT('Ctrl Pts',(0.393275036726237,-0.393275036726696,
1.17551763482278));
#16940=CARTESIAN_POINT('Ctrl Pts',(0.349270066586393,-0.437280006866568,
1.17551763482278));
#16941=CARTESIAN_POINT('Ctrl Pts',(0.31116668672527,-0.492966510304154,
1.17344391775674));
#16942=CARTESIAN_POINT('Ctrl Pts',(0.260619583352803,-0.614748859331208,
1.16502989619586));
#16943=CARTESIAN_POINT('Ctrl Pts',(0.248170686679517,-0.680842516168625,
1.15868899091381));
#16944=CARTESIAN_POINT('Ctrl Pts',(0.248000617699059,-0.743096462400057,
1.15133505381795));
#16945=CARTESIAN_POINT('Ctrl Pts',(0.248000000194873,-0.743548129196139,
1.15128162561027));
#16946=CARTESIAN_POINT('Ctrl Pts',(0.248000000194874,-0.744000000196067,
1.15122809938321));
#16947=CARTESIAN_POINT('',(0.30305692886038,-0.516876228118955,0.19));
#16948=CARTESIAN_POINT('Origin',(0.744000000194874,-0.744000000195115,0.19));
#16949=CARTESIAN_POINT('',(0.248000000194874,-0.744000000196067,0.5833899128444));
#16950=CARTESIAN_POINT('Origin',(0.744000000194874,-0.744000000195115,0.583389912841405));
#16951=CARTESIAN_POINT('',(0.248000000194874,-0.744000000196067,1.2));
#16952=CARTESIAN_POINT('Origin',(0.248000000193922,-0.248000000194471,1.2));
#16953=CARTESIAN_POINT('',(0.248000000195456,-1.04682989872316,1.10790668314425));
#16954=CARTESIAN_POINT('Origin',(0.248000000193446,4.75999652275667E-13,
-5.12965591734105));
#16955=CARTESIAN_POINT('',(0.248000000195353,-0.993500000024651,1.01553658903593));
#16956=CARTESIAN_POINT('Origin',(-1.10000000000019,0.248000000196221,1.2));
#16957=CARTESIAN_POINT('',(-1.04682989872296,0.248000000196221,1.10790668314426));
#16958=CARTESIAN_POINT('Origin',(7.17605422133295E-15,0.248000000196221,
-5.12965591734105));
#16959=CARTESIAN_POINT('',(-1.10000000000019,0.248000000196221,1.2));
#16960=CARTESIAN_POINT('Origin',(-1.10000000000019,-0.248000000195508,1.2));
#16961=CARTESIAN_POINT('',(-1.04942373620595,-1.28517341949389E-16,1.11239934145138));
#16962=CARTESIAN_POINT('Origin',(1.91582141081578,-5.36035544273609E-16,
-4.02355591008731));
#16963=CARTESIAN_POINT('',(-0.516876228118667,-0.124000000097755,0.19));
#16964=CARTESIAN_POINT('Origin',(1.91582141081578,-5.36035544273609E-16,
-4.02355591008731));
#16965=CARTESIAN_POINT('Origin',(-0.248000000196409,-1.09999999999961,1.2));
#16966=CARTESIAN_POINT('',(-0.24800000019626,-1.04682989872243,1.10790668314434));
#16967=CARTESIAN_POINT('Origin',(-0.248000000193338,6.92337424395539E-13,
-5.12965591734105));
#16968=CARTESIAN_POINT('',(-0.248000000196409,-1.09999999999954,1.19999999999987));
#16969=CARTESIAN_POINT('Origin',(0.248000000195558,-1.10000000000039,1.2));
#16970=CARTESIAN_POINT('Origin',(3.00794342650252E-12,1.91582141081592,
-4.02355591008723));
#16971=CARTESIAN_POINT('',(0.124000000097801,-0.516876228118675,0.19));
#16972=CARTESIAN_POINT('Origin',(-5.91193760612896E-14,-1.66533453693773E-15,
0.19));
#16973=CARTESIAN_POINT('Origin',(0.,0.,-0.1));
#16974=CARTESIAN_POINT('',(0.939230484541328,-1.15022560655515E-16,0.));
#16975=CARTESIAN_POINT('Origin',(0.,0.,0.));
#16976=CARTESIAN_POINT('',(0.839230484541328,-1.02776092664042E-16,-0.1));
#16977=CARTESIAN_POINT('Origin',(0.939230484541328,-1.15022560655515E-16,
-0.1));
#16978=CARTESIAN_POINT('Origin',(0.,0.,-0.1));
#16979=CARTESIAN_POINT('Origin',(-0.839230484541328,0.,-7.24797437703358E-18));
#16980=CARTESIAN_POINT('',(2.15,-2.63299061816681E-16,0.));
#16981=CARTESIAN_POINT('Origin',(0.,0.,0.));
#16982=CARTESIAN_POINT('Origin',(0.,0.,-0.0749999999999998));
#16983=CARTESIAN_POINT('',(0.839230484541328,-1.02776092664042E-16,-0.15));
#16984=CARTESIAN_POINT('Origin',(0.,0.,-0.15));
#16985=CARTESIAN_POINT('',(0.839230484541328,-1.02776092664042E-16,-0.0749999999999998));
#16986=CARTESIAN_POINT('Origin',(0.,0.,-0.45));
#16987=CARTESIAN_POINT('',(0.96675,-1.1839272930757E-16,-0.625909310648334));
#16988=CARTESIAN_POINT('Origin',(0.,0.,-0.625909310648334));
#16989=CARTESIAN_POINT('',(0.919615242270664,-1.12620386289389E-16,-0.45));
#16990=CARTESIAN_POINT('Origin',(0.,0.,-3.375));
#16991=CARTESIAN_POINT('',(0.96675,1.1839272930757E-16,-6.));
#16992=CARTESIAN_POINT('Origin',(0.,0.,-6.));
#16993=CARTESIAN_POINT('',(0.96675,-1.1839272930757E-16,-3.375));
#16994=CARTESIAN_POINT('Origin',(0.,0.,-6.));
#16995=CARTESIAN_POINT('Origin',(7.21644966006352E-15,0.,-5.12965591734105));
#16996=CARTESIAN_POINT('',(-2.07563463599418,0.,0.85));
#16997=CARTESIAN_POINT('Origin',(7.21644966006352E-15,0.,-5.12965591734105));
#16998=CARTESIAN_POINT('',(2.07563463599418,-2.54191931316966E-16,0.85));
#16999=CARTESIAN_POINT('Origin',(0.,0.,0.85));
#17000=CARTESIAN_POINT('Origin',(0.,0.,0.85));
#17001=CARTESIAN_POINT('Origin',(0.,0.,0.425));
#17002=CARTESIAN_POINT('',(2.11281731799709,-2.58745496566823E-16,0.425));
#17027=UNCERTAINTY_MEASURE_WITH_UNIT(LENGTH_MEASURE(0.01),#17043,
'DISTANCE_ACCURACY_VALUE',
'Maximum model space distance between geometric entities at asserted c
onnectivities');
#17028=UNCERTAINTY_MEASURE_WITH_UNIT(LENGTH_MEASURE(0.01),#17043,
'DISTANCE_ACCURACY_VALUE',
'Maximum model space distance between geometric entities at asserted c
onnectivities');
#17041=(
GEOMETRIC_REPRESENTATION_CONTEXT(3)
GLOBAL_UNCERTAINTY_ASSIGNED_CONTEXT((#17027))
GLOBAL_UNIT_ASSIGNED_CONTEXT((#17043,#17045,#17046))
REPRESENTATION_CONTEXT('','3D')
);
#17042=(
GEOMETRIC_REPRESENTATION_CONTEXT(3)
GLOBAL_UNCERTAINTY_ASSIGNED_CONTEXT((#17028))
GLOBAL_UNIT_ASSIGNED_CONTEXT((#17043,#17045,#17046))
REPRESENTATION_CONTEXT('','3D')
);
#17043=(
LENGTH_UNIT()
NAMED_UNIT(*)
SI_UNIT(.MILLI.,.METRE.)
);
#17045=(
NAMED_UNIT(*)
PLANE_ANGLE_UNIT()
SI_UNIT($,.RADIAN.)
);
#17046=(
NAMED_UNIT(*)
SI_UNIT($,.STERADIAN.)
SOLID_ANGLE_UNIT()
);
#17059=SHAPE_DEFINITION_REPRESENTATION(#17072,#17097);
#17072=PRODUCT_DEFINITION_SHAPE('',$,#17111);
#17097=SHAPE_REPRESENTATION('',(#9178),#17041);
#17098=PRODUCT_DEFINITION_CONTEXT('part definition',#17139,'design');
#17111=PRODUCT_DEFINITION('BHS JIS B 1111 - M2x6 Steel 4.6 Plain_3',
'Binding Head Screw JIS B 1111 - M2x6 Steel 4.6 Plain v1 (1)',#17124,#17098);
#17124=PRODUCT_DEFINITION_FORMATION('',$,#17153);
#17139=APPLICATION_CONTEXT(
'Core Data for Automotive Mechanical Design Process');
#17140=PRODUCT_CONTEXT('part definition',#17139,'mechanical');
#17153=PRODUCT('BHS JIS B 1111 - M2x6 Steel 4.6 Plain_3',
'Binding Head Screw JIS B 1111 - M2x6 Steel 4.6 Plain v1 (1)',
'Binding Head Screw JIS B 1111 - M2x6',(#17140));
#17154=PRESENTATION_STYLE_ASSIGNMENT((#17155));
#17155=SURFACE_STYLE_USAGE(.BOTH.,#17156);
#17156=SURFACE_SIDE_STYLE('',(#17157));
#17157=SURFACE_STYLE_FILL_AREA(#17158);
#17158=FILL_AREA_STYLE('Steel - Satin',(#17159));
#17159=FILL_AREA_STYLE_COLOUR('Steel - Satin',#17160);
#17160=COLOUR_RGB('Steel - Satin', 0.09019608, 0.27058824, 0.51372549);
ENDSEC;
END-ISO-10303-21;
